ISO-10303-21;
HEADER;
FILE_DESCRIPTION (('STEP AP214'),
    '1' );
FILE_NAME ('Glass Cover.step',
    '2026-10-07T18:46:32',
    ( '' ),
    ( '' ),
    'SwSTEP 2.0',
    'SolidWorks 2020',
    '' );
FILE_SCHEMA (( 'AUTOMOTIVE_DESIGN' ));
ENDSEC;

DATA;
#7=ORIENTED_EDGE ( 'NONE', *, *, #4802, .F. ) ;
#12=CIRCLE ( 'NONE', #12500, 0.2500000000000002220 ) ;
#30=CARTESIAN_POINT ( 'NONE',  ( 14.96174975910705918, 51.61873716947361856, 13.75000000000000000 ) ) ;
#58=DIRECTION ( 'NONE',  ( 1.000000000000000000, 0.000000000000000000, 0.000000000000000000 ) ) ;
#61=DIRECTION ( 'NONE',  ( -1.000000000000000000, -0.000000000000000000, 0.000000000000000000 ) ) ;
#138=ORIENTED_EDGE ( 'NONE', *, *, #854, .T. ) ;
#140=FACE_OUTER_BOUND ( 'NONE', #8226, .T. ) ;
#210=ORIENTED_EDGE ( 'NONE', *, *, #17092, .T. ) ;
#211=EDGE_CURVE ( 'NONE', #1488, #12157, #8148, .T. ) ;
#264=CLOSED_SHELL ( 'NONE', ( #4139, #16179, #15323, #8693, #14959, #1658, #17591, #6091, #17555, #5561, #13125, #9357, #12865, #10102, #11748, #5840, #20555, #6272 ) ) ;
#278=VECTOR ( 'NONE', #5451, 1000.000000000000000 ) ;
#280=EDGE_CURVE ( 'NONE', #2743, #17175, #7794, .T. ) ;
#295=VECTOR ( 'NONE', #10814, 1000.000000000000000 ) ;
#356=EDGE_CURVE ( 'NONE', #2819, #12212, #20621, .T. ) ;
#400=FACE_OUTER_BOUND ( 'NONE', #3553, .T. ) ;
#405=EDGE_LOOP ( 'NONE', ( #18020, #19972, #1126, #15256, #10845, #11379 ) ) ;
#419=APPLICATION_CONTEXT ( 'automotive_design' ) ;
#422=AXIS2_PLACEMENT_3D ( 'NONE', #13047, #1095, #7941 ) ;
#469=MECHANICAL_DESIGN_GEOMETRIC_PRESENTATION_REPRESENTATION('',(#7640),#17639);
#490=PRODUCT_DEFINITION_FORMATION_WITH_SPECIFIED_SOURCE ( 'ANY', '', #16590, .NOT_KNOWN. ) ;
#495=CARTESIAN_POINT ( 'NONE',  ( -14.71174975910705029, 51.61873716947361856, 68.50000000000000000 ) ) ;
#515=CARTESIAN_POINT ( 'NONE',  ( -14.96174975910705207, 50.19799549595485644, 68.25000000000000000 ) ) ;
#520=EDGE_CURVE ( 'NONE', #17175, #17812, #16715, .T. ) ;
#576=CIRCLE ( 'NONE', #13087, 0.5000000000000004441 ) ;
#643=VECTOR ( 'NONE', #15409, 1000.000000000000000 ) ;
#693=CIRCLE ( 'NONE', #3582, 0.2500000000000002220 ) ;
#735=FACE_OUTER_BOUND ( 'NONE', #7826, .T. ) ;
#768=DIRECTION ( 'NONE',  ( 0.000000000000000000, 0.000000000000000000, 1.000000000000000000 ) ) ;
#854=EDGE_CURVE ( 'NONE', #6442, #21823, #693, .T. ) ;
#888=AXIS2_PLACEMENT_3D ( 'NONE', #8018, #9255, #14482 ) ;
#1009=DIRECTION ( 'NONE',  ( -0.000000000000000000, -1.000000000000000000, 0.000000000000000000 ) ) ;
#1021=ORIENTED_EDGE ( 'NONE', *, *, #16712, .T. ) ;
#1095=DIRECTION ( 'NONE',  ( 0.000000000000000000, 1.000000000000000000, -0.000000000000000000 ) ) ;
#1106=VECTOR ( 'NONE', #1009, 1000.000000000000000 ) ;
#1126=ORIENTED_EDGE ( 'NONE', *, *, #14675, .T. ) ;
#1131=EDGE_LOOP ( 'NONE', ( #5506, #6483, #9261, #21023, #17043, #11707, #1139, #7153 ) ) ;
#1139=ORIENTED_EDGE ( 'NONE', *, *, #12018, .T. ) ;
#1177=VERTEX_POINT ( 'NONE', #2629 ) ;
#1216=EDGE_CURVE ( 'NONE', #12212, #1750, #21225, .T. ) ;
#1237=DIRECTION ( 'NONE',  ( 0.000000000000000000, 0.000000000000000000, 1.000000000000000000 ) ) ;
#1246=CARTESIAN_POINT ( 'NONE',  ( 14.96174975910707161, 51.86873716947361856, 68.00000000000000000 ) ) ;
#1334=AXIS2_PLACEMENT_3D ( 'NONE', #8386, #10299, #20043 ) ;
#1355=CIRCLE ( 'NONE', #14930, 0.2500000000000002220 ) ;
#1368=( NAMED_UNIT ( * ) PLANE_ANGLE_UNIT ( ) SI_UNIT ( $, .RADIAN. ) );
#1397=CYLINDRICAL_SURFACE ( 'NONE', #12672, 0.5000000000000004441 ) ;
#1488=VERTEX_POINT ( 'NONE', #4244 ) ;
#1532=CARTESIAN_POINT ( 'NONE',  ( 14.71174975910705740, 50.19799549595485644, 13.50000000000000000 ) ) ;
#1545=VERTEX_POINT ( 'NONE', #11824 ) ;
#1596=EDGE_LOOP ( 'NONE', ( #21372, #3792, #6050, #3016 ) ) ;
#1636=CARTESIAN_POINT ( 'NONE',  ( -14.96174975910705207, 51.86873716947361856, 13.05380965755523448 ) ) ;
#1649=CIRCLE ( 'NONE', #7021, 0.5000000000000004441 ) ;
#1658=ADVANCED_FACE ( 'NONE', ( #10280 ), #20569, .T. ) ;
#1714=( NAMED_UNIT ( * ) SI_UNIT ( $, .STERADIAN. ) SOLID_ANGLE_UNIT ( ) );
#1723=ORIENTED_EDGE ( 'NONE', *, *, #6142, .F. ) ;
#1750=VERTEX_POINT ( 'NONE', #20794 ) ;
#1777=CARTESIAN_POINT ( 'NONE',  ( -14.96174975910705207, 32.10873716947361345, 68.25000000000000000 ) ) ;
#1890=FACE_OUTER_BOUND ( 'NONE', #20607, .T. ) ;
#1942=DIRECTION ( 'NONE',  ( 0.000000000000000000, 0.000000000000000000, 1.000000000000000000 ) ) ;
#2099=VERTEX_POINT ( 'NONE', #13914 ) ;
#2140=DIRECTION ( 'NONE',  ( -1.000000000000000000, 0.000000000000000000, 0.000000000000000000 ) ) ;
#2154=CARTESIAN_POINT ( 'NONE',  ( -14.71174975910705029, 51.61873716947361856, 14.00000000000000000 ) ) ;
#2207=LINE ( 'NONE', #21019, #6625 ) ;
#2232=DIRECTION ( 'NONE',  ( 1.000000000000000000, 0.000000000000000000, -2.388292521039847891E-16 ) ) ;
#2248=CARTESIAN_POINT ( 'NONE',  ( -14.96174975910705207, 51.61873716947361856, 68.00000000000000000 ) ) ;
#2264=EDGE_LOOP ( 'NONE', ( #1021, #18937, #21411, #2525 ) ) ;
#2417=DIRECTION ( 'NONE',  ( -1.000000000000000000, -0.000000000000000000, 0.000000000000000000 ) ) ;
#2458=FACE_OUTER_BOUND ( 'NONE', #2264, .T. ) ;
#2464=PRODUCT_CONTEXT ( 'NONE', #419, 'mechanical' ) ;
#2469=VERTEX_POINT ( 'NONE', #7004 ) ;
#2525=ORIENTED_EDGE ( 'NONE', *, *, #14675, .F. ) ;
#2539=CARTESIAN_POINT ( 'NONE',  ( 14.96174975910705918, 50.19799549595485644, 13.75000000000000000 ) ) ;
#2564=EDGE_CURVE ( 'NONE', #5916, #5378, #8451, .T. ) ;
#2606=DIRECTION ( 'NONE',  ( 2.388292521039847891E-16, 0.000000000000000000, 1.000000000000000000 ) ) ;
#2624=CARTESIAN_POINT ( 'NONE',  ( 15.95292532278785913, 51.61873716947361856, 13.50000000000000000 ) ) ;
#2629=CARTESIAN_POINT ( 'NONE',  ( 14.96174975910707161, 50.19799549595485644, 68.25000000000000000 ) ) ;
#2687=LINE ( 'NONE', #9519, #1106 ) ;
#2743=VERTEX_POINT ( 'NONE', #20761 ) ;
#2771=TOROIDAL_SURFACE ( 'NONE', #12744, 0.2500000000000000000, 0.2500000000000000000 ) ;
#2819=VERTEX_POINT ( 'NONE', #1246 ) ;
#2835=ORIENTED_EDGE ( 'NONE', *, *, #17544, .T. ) ;
#2924=LINE ( 'NONE', #4271, #10158 ) ;
#2959=DIRECTION ( 'NONE',  ( 0.000000000000000000, 0.000000000000000000, 1.000000000000000000 ) ) ;
#2999=EDGE_CURVE ( 'NONE', #11094, #18906, #11771, .T. ) ;
#3016=ORIENTED_EDGE ( 'NONE', *, *, #2564, .F. ) ;
#3075=ORIENTED_EDGE ( 'NONE', *, *, #19116, .F. ) ;
#3088=ORIENTED_EDGE ( 'NONE', *, *, #17186, .F. ) ;
#3097=EDGE_CURVE ( 'NONE', #1750, #9565, #21734, .T. ) ;
#3107=DIRECTION ( 'NONE',  ( -1.000000000000000000, 0.000000000000000000, 0.000000000000000000 ) ) ;
#3116=CARTESIAN_POINT ( 'NONE',  ( -0.000000000000000000, 51.61873716947361856, 68.50000000000000000 ) ) ;
#3117=CIRCLE ( 'NONE', #20630, 0.2500000000000002220 ) ;
#3199=EDGE_CURVE ( 'NONE', #19660, #12157, #2924, .T. ) ;
#3252=FACE_OUTER_BOUND ( 'NONE', #7984, .T. ) ;
#3340=DIRECTION ( 'NONE',  ( -2.388292521039847891E-16, 0.000000000000000000, -1.000000000000000000 ) ) ;
#3343=DIRECTION ( 'NONE',  ( -0.000000000000000000, 1.000000000000000000, -0.000000000000000000 ) ) ;
#3379=DIRECTION ( 'NONE',  ( 0.000000000000000000, 1.000000000000000000, -0.000000000000000000 ) ) ;
#3425=CARTESIAN_POINT ( 'NONE',  ( -14.96174975910705207, 51.61873716947361856, 14.00000000000000000 ) ) ;
#3501=DIRECTION ( 'NONE',  ( 0.000000000000000000, -0.000000000000000000, 1.000000000000000000 ) ) ;
#3520=AXIS2_PLACEMENT_3D ( 'NONE', #15342, #15219, #18473 ) ;
#3553=EDGE_LOOP ( 'NONE', ( #8858, #13895, #9021, #19310 ) ) ;
#3567=CARTESIAN_POINT ( 'NONE',  ( 14.96174975910705918, 32.10873716947361345, 13.05380965755522737 ) ) ;
#3582=AXIS2_PLACEMENT_3D ( 'NONE', #21698, #12604, #3107 ) ;
#3615=DIRECTION ( 'NONE',  ( 0.000000000000000000, -1.000000000000000000, -0.000000000000000000 ) ) ;
#3756=CARTESIAN_POINT ( 'NONE',  ( 14.96174975910705918, 51.86873716947361856, 13.05380965755522737 ) ) ;
#3779=EDGE_CURVE ( 'NONE', #12641, #21318, #21770, .T. ) ;
#3792=ORIENTED_EDGE ( 'NONE', *, *, #9151, .F. ) ;
#3835=DIRECTION ( 'NONE',  ( 0.000000000000000000, 0.000000000000000000, 1.000000000000000000 ) ) ;
#3850=ORIENTED_EDGE ( 'NONE', *, *, #4592, .F. ) ;
#3916=EDGE_CURVE ( 'NONE', #12157, #12641, #8379, .T. ) ;
#3924=AXIS2_PLACEMENT_3D ( 'NONE', #11851, #10184, #6852 ) ;
#4014=ORIENTED_EDGE ( 'NONE', *, *, #5879, .T. ) ;
#4020=ORIENTED_EDGE ( 'NONE', *, *, #1216, .F. ) ;
#4080=EDGE_LOOP ( 'NONE', ( #8945, #7643, #6808, #17593 ) ) ;
#4091=DIRECTION ( 'NONE',  ( 1.000000000000000000, 0.000000000000000000, 0.000000000000000000 ) ) ;
#4111=CARTESIAN_POINT ( 'NONE',  ( -14.71174975910705029, 0.000000000000000000, 68.25000000000000000 ) ) ;
#4137=CARTESIAN_POINT ( 'NONE',  ( 14.71174975910705740, 51.61873716947361856, 13.50000000000000000 ) ) ;
#4139=ADVANCED_FACE ( 'NONE', ( #12596 ), #19439, .T. ) ;
#4203=CARTESIAN_POINT ( 'NONE',  ( -14.71174975910705029, 50.19799549595485644, 13.50000000000000000 ) ) ;
#4225=DIRECTION ( 'NONE',  ( 0.000000000000000000, -1.000000000000000000, -0.000000000000000000 ) ) ;
#4244=CARTESIAN_POINT ( 'NONE',  ( -14.71174975910705029, 50.19799549595485644, 68.50000000000000000 ) ) ;
#4271=CARTESIAN_POINT ( 'NONE',  ( -14.96174975910705207, 50.19799549595485644, -3.500000000000003109 ) ) ;
#4274=EDGE_CURVE ( 'NONE', #1545, #2819, #12753, .T. ) ;
#4538=VECTOR ( 'NONE', #10237, 1000.000000000000000 ) ;
#4552=ORIENTED_EDGE ( 'NONE', *, *, #2999, .F. ) ;
#4582=CARTESIAN_POINT ( 'NONE',  ( -14.71174975910705029, 51.61873716947361856, 68.25000000000000000 ) ) ;
#4592=EDGE_CURVE ( 'NONE', #6442, #2469, #5016, .T. ) ;
#4609=CARTESIAN_POINT ( 'NONE',  ( -15.95292532278785913, 52.11873716947361856, 14.00000000000000000 ) ) ;
#4802=EDGE_CURVE ( 'NONE', #5916, #1488, #9244, .T. ) ;
#4889=ORIENTED_EDGE ( 'NONE', *, *, #14414, .F. ) ;
#4907=CARTESIAN_POINT ( 'NONE',  ( -14.96174975910705207, 51.61873716947361856, 68.25000000000000000 ) ) ;
#4909=FACE_OUTER_BOUND ( 'NONE', #18635, .T. ) ;
#4982=EDGE_CURVE ( 'NONE', #18731, #17175, #16803, .T. ) ;
#5016=LINE ( 'NONE', #1636, #643 ) ;
#5095=CARTESIAN_POINT ( 'NONE',  ( -14.71174975910705029, 0.000000000000000000, 68.50000000000000000 ) ) ;
#5105=CARTESIAN_POINT ( 'NONE',  ( 0.000000000000000000, 51.61873716947361856, 14.00000000000000000 ) ) ;
#5123=EDGE_CURVE ( 'NONE', #5378, #12212, #1649, .T. ) ;
#5156=CYLINDRICAL_SURFACE ( 'NONE', #3924, 0.5000000000000004441 ) ;
#5158=AXIS2_PLACEMENT_3D ( 'NONE', #3567, #16630, #5576 ) ;
#5169=FACE_OUTER_BOUND ( 'NONE', #6126, .T. ) ;
#5191=PRESENTATION_STYLE_ASSIGNMENT (( #20523 ) ) ;
#5210=CARTESIAN_POINT ( 'NONE',  ( -14.71174975910705029, 51.86873716947361856, 109.6002446535588319 ) ) ;
#5267=CIRCLE ( 'NONE', #15258, 0.2500000000000002220 ) ;
#5320=( LENGTH_UNIT ( ) NAMED_UNIT ( * ) SI_UNIT ( .MILLI., .METRE. ) );
#5378=VERTEX_POINT ( 'NONE', #22057 ) ;
#5447=VECTOR ( 'NONE', #6013, 1000.000000000000000 ) ;
#5451=DIRECTION ( 'NONE',  ( 2.388292521039847891E-16, -0.000000000000000000, 1.000000000000000000 ) ) ;
#5476=CARTESIAN_POINT ( 'NONE',  ( 0.000000000000000000, 0.000000000000000000, 68.50000000000000000 ) ) ;
#5506=ORIENTED_EDGE ( 'NONE', *, *, #211, .T. ) ;
#5561=ADVANCED_FACE ( 'NONE', ( #6801 ), #1397, .T. ) ;
#5574=CARTESIAN_POINT ( 'NONE',  ( 0.000000000000000000, 0.000000000000000000, 13.50000000000000000 ) ) ;
#5576=DIRECTION ( 'NONE',  ( -2.388292521039847891E-16, 0.000000000000000000, -1.000000000000000000 ) ) ;
#5646=DIRECTION ( 'NONE',  ( -1.000000000000000000, 0.000000000000000000, 0.000000000000000000 ) ) ;
#5840=ADVANCED_FACE ( 'NONE', ( #4909 ), #16618, .T. ) ;
#5879=EDGE_CURVE ( 'NONE', #5378, #21318, #6941, .T. ) ;
#5891=DIRECTION ( 'NONE',  ( 0.000000000000000000, -0.000000000000000000, 1.000000000000000000 ) ) ;
#5900=CYLINDRICAL_SURFACE ( 'NONE', #17120, 0.2500000000000002220 ) ;
#5916=VERTEX_POINT ( 'NONE', #16977 ) ;
#6013=DIRECTION ( 'NONE',  ( -2.388292521039847891E-16, 0.000000000000000000, -1.000000000000000000 ) ) ;
#6050=ORIENTED_EDGE ( 'NONE', *, *, #16425, .T. ) ;
#6062=SHAPE_DEFINITION_REPRESENTATION ( #21629, #6277 ) ;
#6091=ADVANCED_FACE ( 'NONE', ( #7258 ), #20797, .T. ) ;
#6095=COLOUR_RGB ( '', 0.72549020, 0.75294118, 0.79215686) ;
#6122=LINE ( 'NONE', #16255, #11353 ) ;
#6126=EDGE_LOOP ( 'NONE', ( #6169, #7014, #13291, #14291 ) ) ;
#6127=DIRECTION ( 'NONE',  ( 1.000000000000000000, 0.000000000000000000, -2.388292521039847891E-16 ) ) ;
#6142=EDGE_CURVE ( 'NONE', #2469, #9565, #12313, .T. ) ;
#6169=ORIENTED_EDGE ( 'NONE', *, *, #3779, .T. ) ;
#6272=ADVANCED_FACE ( 'NONE', ( #16729 ), #20203, .F. ) ;
#6277=SHAPE_REPRESENTATION ( 'Glass Cover', ( #17493 ), #19794 ) ;
#6315=FILL_AREA_STYLE_COLOUR ( '', #6095 ) ;
#6327=ORIENTED_EDGE ( 'NONE', *, *, #211, .F. ) ;
#6442=VERTEX_POINT ( 'NONE', #18976 ) ;
#6483=ORIENTED_EDGE ( 'NONE', *, *, #3199, .F. ) ;
#6488=AXIS2_PLACEMENT_3D ( 'NONE', #13669, #18828, #3501 ) ;
#6603=ORIENTED_EDGE ( 'NONE', *, *, #3916, .T. ) ;
#6613=DIRECTION ( 'NONE',  ( 0.000000000000000000, 0.000000000000000000, -1.000000000000000000 ) ) ;
#6625=VECTOR ( 'NONE', #9257, 1000.000000000000000 ) ;
#6637=ORIENTED_EDGE ( 'NONE', *, *, #7214, .F. ) ;
#6801=FACE_OUTER_BOUND ( 'NONE', #12373, .T. ) ;
#6808=ORIENTED_EDGE ( 'NONE', *, *, #17186, .T. ) ;
#6835=DIRECTION ( 'NONE',  ( 1.000000000000000000, 0.000000000000000000, -2.388292521039847891E-16 ) ) ;
#6852=DIRECTION ( 'NONE',  ( 0.000000000000000000, 0.000000000000000000, -1.000000000000000000 ) ) ;
#6912=DIRECTION ( 'NONE',  ( 0.000000000000000000, 0.000000000000000000, 1.000000000000000000 ) ) ;
#6941=LINE ( 'NONE', #3116, #15882 ) ;
#7004=CARTESIAN_POINT ( 'NONE',  ( -14.96174975910705207, 51.86873716947361856, 14.00000000000000000 ) ) ;
#7014=ORIENTED_EDGE ( 'NONE', *, *, #19930, .F. ) ;
#7021=AXIS2_PLACEMENT_3D ( 'NONE', #8973, #19270, #10762 ) ;
#7120=FACE_OUTER_BOUND ( 'NONE', #20429, .T. ) ;
#7153=ORIENTED_EDGE ( 'NONE', *, *, #4802, .T. ) ;
#7162=ORIENTED_EDGE ( 'NONE', *, *, #356, .F. ) ;
#7209=( LENGTH_UNIT ( ) NAMED_UNIT ( * ) SI_UNIT ( .MILLI., .METRE. ) );
#7214=EDGE_CURVE ( 'NONE', #9565, #21823, #2207, .T. ) ;
#7218=AXIS2_PLACEMENT_3D ( 'NONE', #18917, #16889, #18681 ) ;
#7258=FACE_OUTER_BOUND ( 'NONE', #14678, .T. ) ;
#7400=ORIENTED_EDGE ( 'NONE', *, *, #5879, .F. ) ;
#7466=CARTESIAN_POINT ( 'NONE',  ( 14.71174975910707161, 51.86873716947361856, 68.00000000000000000 ) ) ;
#7489=ORIENTED_EDGE ( 'NONE', *, *, #14414, .T. ) ;
#7570=CIRCLE ( 'NONE', #21524, 0.2500000000000002220 ) ;
#7640=STYLED_ITEM ( 'NONE', ( #5191 ), #16315 ) ;
#7643=ORIENTED_EDGE ( 'NONE', *, *, #7214, .T. ) ;
#7674=CARTESIAN_POINT ( 'NONE',  ( -14.96174975910705207, 50.19799549595485644, 68.50000000000000000 ) ) ;
#7794=CIRCLE ( 'NONE', #20292, 0.2500000000000002220 ) ;
#7825=AXIS2_PLACEMENT_3D ( 'NONE', #5574, #12357, #19213 ) ;
#7826=EDGE_LOOP ( 'NONE', ( #210, #4020, #7162, #11633 ) ) ;
#7887=CARTESIAN_POINT ( 'NONE',  ( -14.96174975910705207, 32.10873716947361345, 13.05380965755523448 ) ) ;
#7941=DIRECTION ( 'NONE',  ( 0.000000000000000000, 0.000000000000000000, 1.000000000000000000 ) ) ;
#7966=CARTESIAN_POINT ( 'NONE',  ( 14.96174975910707161, 32.10873716947361345, 68.25000000000000000 ) ) ;
#7984=EDGE_LOOP ( 'NONE', ( #3088, #15728, #7400, #15236 ) ) ;
#7988=FILL_AREA_STYLE ('',( #6315 ) ) ;
#8018=CARTESIAN_POINT ( 'NONE',  ( -14.71174975910705029, 51.86873716947361856, 14.00000000000000000 ) ) ;
#8109=ORIENTED_EDGE ( 'NONE', *, *, #8719, .F. ) ;
#8126=CARTESIAN_POINT ( 'NONE',  ( -14.71174975910705029, 51.61873716947361856, 68.00000000000000000 ) ) ;
#8141=VECTOR ( 'NONE', #10345, 1000.000000000000000 ) ;
#8148=CIRCLE ( 'NONE', #1334, 0.2500000000000002220 ) ;
#8226=EDGE_LOOP ( 'NONE', ( #11577, #4889, #11133, #12522 ) ) ;
#8236=DIRECTION ( 'NONE',  ( 1.000000000000000000, -0.000000000000000000, -0.000000000000000000 ) ) ;
#8287=CARTESIAN_POINT ( 'NONE',  ( -14.71174975910705029, 51.61873716947361856, 13.75000000000000000 ) ) ;
#8362=ORIENTED_EDGE ( 'NONE', *, *, #4592, .T. ) ;
#8379=LINE ( 'NONE', #1777, #14957 ) ;
#8386=CARTESIAN_POINT ( 'NONE',  ( -14.71174975910705029, 50.19799549595485644, 68.25000000000000000 ) ) ;
#8388=CYLINDRICAL_SURFACE ( 'NONE', #7218, 0.2500000000000002220 ) ;
#8406=DIRECTION ( 'NONE',  ( -1.000000000000000000, 0.000000000000000000, 0.000000000000000000 ) ) ;
#8412=PRODUCT_DEFINITION_CONTEXT ( 'detailed design', #13849, 'design' ) ;
#8451=LINE ( 'NONE', #20199, #13264 ) ;
#8454=VERTEX_POINT ( 'NONE', #1532 ) ;
#8528=FACE_OUTER_BOUND ( 'NONE', #1596, .T. ) ;
#8617=DIRECTION ( 'NONE',  ( 8.326672684688666480E-14, 0.000000000000000000, 1.000000000000000000 ) ) ;
#8693=ADVANCED_FACE ( 'NONE', ( #400 ), #20896, .F. ) ;
#8697=DIRECTION ( 'NONE',  ( -1.000000000000000000, 0.000000000000000000, 0.000000000000000000 ) ) ;
#8719=EDGE_CURVE ( 'NONE', #2819, #2099, #19974, .T. ) ;
#8725=ORIENTED_EDGE ( 'NONE', *, *, #16712, .F. ) ;
#8858=ORIENTED_EDGE ( 'NONE', *, *, #20828, .T. ) ;
#8945=ORIENTED_EDGE ( 'NONE', *, *, #3097, .T. ) ;
#8973=CARTESIAN_POINT ( 'NONE',  ( 14.71174975910707161, 51.61873716947361856, 68.00000000000000000 ) ) ;
#9021=ORIENTED_EDGE ( 'NONE', *, *, #4982, .T. ) ;
#9036=DIRECTION ( 'NONE',  ( -1.000000000000000000, 0.000000000000000000, 0.000000000000000000 ) ) ;
#9062=DIRECTION ( 'NONE',  ( -2.388292521039847891E-16, 0.000000000000000000, -1.000000000000000000 ) ) ;
#9151=EDGE_CURVE ( 'NONE', #2099, #1177, #10886, .T. ) ;
#9229=TOROIDAL_SURFACE ( 'NONE', #21032, 0.2500000000000000000, 0.2500000000000000000 ) ;
#9244=LINE ( 'NONE', #7674, #295 ) ;
#9255=DIRECTION ( 'NONE',  ( 0.000000000000000000, 0.000000000000000000, -1.000000000000000000 ) ) ;
#9257=DIRECTION ( 'NONE',  ( 0.000000000000000000, 0.000000000000000000, 1.000000000000000000 ) ) ;
#9261=ORIENTED_EDGE ( 'NONE', *, *, #20465, .T. ) ;
#9294=VECTOR ( 'NONE', #2606, 1000.000000000000000 ) ;
#9357=ADVANCED_FACE ( 'NONE', ( #3252 ), #5156, .T. ) ;
#9440=CARTESIAN_POINT ( 'NONE',  ( 14.96174975910705918, 51.61873716947361856, 14.00000000000000000 ) ) ;
#9455=CARTESIAN_POINT ( 'NONE',  ( 14.71174975910708049, 52.11873716947361856, 109.6002446535588319 ) ) ;
#9519=CARTESIAN_POINT ( 'NONE',  ( 14.71174975910705740, 42.31054587065082728, 13.50000000000000000 ) ) ;
#9565=VERTEX_POINT ( 'NONE', #13610 ) ;
#9672=CARTESIAN_POINT ( 'NONE',  ( 14.96174975910705918, 50.19799549595485644, 13.05380965755522737 ) ) ;
#9738=ORIENTED_EDGE ( 'NONE', *, *, #520, .F. ) ;
#9750=DIRECTION ( 'NONE',  ( -0.000000000000000000, -1.000000000000000000, -0.000000000000000000 ) ) ;
#9767=CARTESIAN_POINT ( 'NONE',  ( 0.000000000000000000, 0.000000000000000000, 0.000000000000000000 ) ) ;
#9775=( NAMED_UNIT ( * ) SI_UNIT ( $, .STERADIAN. ) SOLID_ANGLE_UNIT ( ) );
#9942=CYLINDRICAL_SURFACE ( 'NONE', #422, 0.2500000000000002220 ) ;
#9956=CARTESIAN_POINT ( 'NONE',  ( 14.71174975910707161, 50.19799549595485644, 68.25000000000000000 ) ) ;
#10094=CARTESIAN_POINT ( 'NONE',  ( 14.71174975910707161, 51.61873716947361856, 68.25000000000000000 ) ) ;
#10097=CYLINDRICAL_SURFACE ( 'NONE', #12422, 0.2500000000000002220 ) ;
#10102=ADVANCED_FACE ( 'NONE', ( #140 ), #16012, .T. ) ;
#10146=ORIENTED_EDGE ( 'NONE', *, *, #19116, .T. ) ;
#10158=VECTOR ( 'NONE', #14542, 1000.000000000000000 ) ;
#10184=DIRECTION ( 'NONE',  ( 1.000000000000000000, 0.000000000000000000, 0.000000000000000000 ) ) ;
#10237=DIRECTION ( 'NONE',  ( 0.000000000000000000, -1.000000000000000000, 0.000000000000000000 ) ) ;
#10264=AXIS2_PLACEMENT_3D ( 'NONE', #10094, #16902, #15338 ) ;
#10280=FACE_OUTER_BOUND ( 'NONE', #405, .T. ) ;
#10299=DIRECTION ( 'NONE',  ( 0.000000000000000000, -1.000000000000000000, -0.000000000000000000 ) ) ;
#10345=DIRECTION ( 'NONE',  ( 1.000000000000000000, 0.000000000000000000, 0.000000000000000000 ) ) ;
#10407=AXIS2_PLACEMENT_3D ( 'NONE', #2248, #2140, #3835 ) ;
#10566=AXIS2_PLACEMENT_3D ( 'NONE', #21791, #22126, #17065 ) ;
#10720=EDGE_LOOP ( 'NONE', ( #20057, #14953, #12379, #14309 ) ) ;
#10762=DIRECTION ( 'NONE',  ( 0.000000000000000000, 0.000000000000000000, -1.000000000000000000 ) ) ;
#10814=DIRECTION ( 'NONE',  ( -1.000000000000000000, -0.000000000000000000, -0.000000000000000000 ) ) ;
#10845=ORIENTED_EDGE ( 'NONE', *, *, #8719, .T. ) ;
#10886=LINE ( 'NONE', #7966, #20013 ) ;
#10906=AXIS2_PLACEMENT_3D ( 'NONE', #11937, #6835, #3340 ) ;
#10939=AXIS2_PLACEMENT_3D ( 'NONE', #19544, #4225, #11042 ) ;
#11042=DIRECTION ( 'NONE',  ( 0.000000000000000000, 0.000000000000000000, 1.000000000000000000 ) ) ;
#11090=EDGE_CURVE ( 'NONE', #8454, #11094, #19171, .T. ) ;
#11094=VERTEX_POINT ( 'NONE', #2539 ) ;
#11133=ORIENTED_EDGE ( 'NONE', *, *, #280, .F. ) ;
#11353=VECTOR ( 'NONE', #21332, 1000.000000000000000 ) ;
#11379=ORIENTED_EDGE ( 'NONE', *, *, #9151, .T. ) ;
#11415=CARTESIAN_POINT ( 'NONE',  ( -14.96174975910705207, 50.19799549595485644, 13.75000000000000000 ) ) ;
#11444=SURFACE_SIDE_STYLE ('',( #19967 ) ) ;
#11577=ORIENTED_EDGE ( 'NONE', *, *, #6142, .T. ) ;
#11580=DIRECTION ( 'NONE',  ( -0.000000000000000000, 1.000000000000000000, 0.000000000000000000 ) ) ;
#11594=FACE_OUTER_BOUND ( 'NONE', #10720, .T. ) ;
#11633=ORIENTED_EDGE ( 'NONE', *, *, #4274, .F. ) ;
#11699=AXIS2_PLACEMENT_3D ( 'NONE', #4111, #17865, #19549 ) ;
#11707=ORIENTED_EDGE ( 'NONE', *, *, #20381, .T. ) ;
#11728=DIRECTION ( 'NONE',  ( 0.000000000000000000, -1.000000000000000000, -0.000000000000000000 ) ) ;
#11748=ADVANCED_FACE ( 'NONE', ( #2458 ), #2771, .T. ) ;
#11771=LINE ( 'NONE', #30, #15097 ) ;
#11824=CARTESIAN_POINT ( 'NONE',  ( 14.96174975910705918, 51.86873716947361856, 14.00000000000000000 ) ) ;
#11851=CARTESIAN_POINT ( 'NONE',  ( 0.000000000000000000, 51.61873716947361856, 68.00000000000000000 ) ) ;
#11888=( NAMED_UNIT ( * ) PLANE_ANGLE_UNIT ( ) SI_UNIT ( $, .RADIAN. ) );
#11937=CARTESIAN_POINT ( 'NONE',  ( 14.71174975910707161, 51.61873716947361856, 68.00000000000000000 ) ) ;
#12018=EDGE_CURVE ( 'NONE', #1177, #5916, #1355, .T. ) ;
#12025=DIRECTION ( 'NONE',  ( 0.000000000000000000, 0.000000000000000000, 1.000000000000000000 ) ) ;
#12157=VERTEX_POINT ( 'NONE', #515 ) ;
#12212=VERTEX_POINT ( 'NONE', #15954 ) ;
#12309=( NAMED_UNIT ( * ) PLANE_ANGLE_UNIT ( ) SI_UNIT ( $, .RADIAN. ) );
#12313=CIRCLE ( 'NONE', #888, 0.2500000000000002220 ) ;
#12336=ORIENTED_EDGE ( 'NONE', *, *, #3779, .F. ) ;
#12357=DIRECTION ( 'NONE',  ( 0.000000000000000000, 0.000000000000000000, 1.000000000000000000 ) ) ;
#12373=EDGE_LOOP ( 'NONE', ( #9738, #7489, #19164, #2835 ) ) ;
#12379=ORIENTED_EDGE ( 'NONE', *, *, #280, .T. ) ;
#12422=AXIS2_PLACEMENT_3D ( 'NONE', #16677, #21961, #18361 ) ;
#12500=AXIS2_PLACEMENT_3D ( 'NONE', #14446, #3615, #18711 ) ;
#12522=ORIENTED_EDGE ( 'NONE', *, *, #16770, .F. ) ;
#12562=ORIENTED_EDGE ( 'NONE', *, *, #18857, .T. ) ;
#12577=VECTOR ( 'NONE', #17801, 1000.000000000000000 ) ;
#12587=DIRECTION ( 'NONE',  ( -2.388292521039847891E-16, 0.000000000000000000, -1.000000000000000000 ) ) ;
#12596=FACE_OUTER_BOUND ( 'NONE', #20987, .T. ) ;
#12604=DIRECTION ( 'NONE',  ( 0.000000000000000000, 0.000000000000000000, -1.000000000000000000 ) ) ;
#12610=COLOUR_RGB ( '', 0.72549020, 0.75294118, 0.79215686) ;
#12641=VERTEX_POINT ( 'NONE', #4907 ) ;
#12672=AXIS2_PLACEMENT_3D ( 'NONE', #5105, #61, #6912 ) ;
#12693=VECTOR ( 'NONE', #3379, 1000.000000000000000 ) ;
#12722=AXIS2_PLACEMENT_3D ( 'NONE', #7466, #5891, #4091 ) ;
#12744=AXIS2_PLACEMENT_3D ( 'NONE', #19358, #2232, #9062 ) ;
#12753=LINE ( 'NONE', #3756, #278 ) ;
#12807=CARTESIAN_POINT ( 'NONE',  ( 14.96174975910707161, 51.61873716947361856, 68.00000000000000000 ) ) ;
#12865=ADVANCED_FACE ( 'NONE', ( #735 ), #5900, .T. ) ;
#12892=DIRECTION ( 'NONE',  ( 1.000000000000000000, 0.000000000000000000, -2.388292521039847891E-16 ) ) ;
#12916=DIRECTION ( 'NONE',  ( 0.000000000000000000, 0.000000000000000000, 1.000000000000000000 ) ) ;
#13016=DIRECTION ( 'NONE',  ( 0.000000000000000000, 0.000000000000000000, -1.000000000000000000 ) ) ;
#13047=CARTESIAN_POINT ( 'NONE',  ( -14.71174975910705029, 32.10873716947361345, 13.75000000000000000 ) ) ;
#13087=AXIS2_PLACEMENT_3D ( 'NONE', #8126, #8236, #12916 ) ;
#13097=UNCERTAINTY_MEASURE_WITH_UNIT (LENGTH_MEASURE( 1.000000000000000082E-05 ), #21644, 'distance_accuracy_value', 'NONE');
#13125=ADVANCED_FACE ( 'NONE', ( #7120 ), #20654, .T. ) ;
#13264=VECTOR ( 'NONE', #13794, 1000.000000000000000 ) ;
#13291=ORIENTED_EDGE ( 'NONE', *, *, #854, .F. ) ;
#13398=DIRECTION ( 'NONE',  ( -1.000000000000000000, -0.000000000000000000, -0.000000000000000000 ) ) ;
#13458=CARTESIAN_POINT ( 'NONE',  ( -14.71174975910705029, 51.61873716947361856, 13.50000000000000000 ) ) ;
#13610=CARTESIAN_POINT ( 'NONE',  ( -14.71174975910705029, 52.11873716947361856, 14.00000000000000000 ) ) ;
#13659=DIRECTION ( 'NONE',  ( 0.000000000000000000, 0.000000000000000000, 1.000000000000000000 ) ) ;
#13669=CARTESIAN_POINT ( 'NONE',  ( 0.000000000000000000, 52.11873716947361856, 109.6002446535588319 ) ) ;
#13678=FILL_AREA_STYLE_COLOUR ( '', #12610 ) ;
#13702=DIRECTION ( 'NONE',  ( 0.000000000000000000, 0.000000000000000000, 1.000000000000000000 ) ) ;
#13766=DIRECTION ( 'NONE',  ( -0.000000000000000000, 1.000000000000000000, 0.000000000000000000 ) ) ;
#13794=DIRECTION ( 'NONE',  ( 0.000000000000000000, 1.000000000000000000, 0.000000000000000000 ) ) ;
#13835=AXIS2_PLACEMENT_3D ( 'NONE', #19980, #2959, #19853 ) ;
#13849=APPLICATION_CONTEXT ( 'automotive_design' ) ;
#13856=UNCERTAINTY_MEASURE_WITH_UNIT (LENGTH_MEASURE( 1.000000000000000082E-05 ), #7209, 'distance_accuracy_value', 'NONE');
#13895=ORIENTED_EDGE ( 'NONE', *, *, #15603, .T. ) ;
#13899=FILL_AREA_STYLE ('',( #13678 ) ) ;
#13914=CARTESIAN_POINT ( 'NONE',  ( 14.96174975910707161, 51.61873716947361856, 68.25000000000000000 ) ) ;
#13929=MECHANICAL_DESIGN_GEOMETRIC_PRESENTATION_REPRESENTATION('',(#15719),#20737);
#14007=DIRECTION ( 'NONE',  ( 0.000000000000000000, 0.000000000000000000, 1.000000000000000000 ) ) ;
#14055=DIRECTION ( 'NONE',  ( -0.000000000000000000, 0.000000000000000000, 1.000000000000000000 ) ) ;
#14291=ORIENTED_EDGE ( 'NONE', *, *, #20614, .F. ) ;
#14309=ORIENTED_EDGE ( 'NONE', *, *, #4982, .F. ) ;
#14380=CARTESIAN_POINT ( 'NONE',  ( 14.71174975910708049, 51.86873716947361856, 109.6002446535588319 ) ) ;
#14414=EDGE_CURVE ( 'NONE', #17175, #9565, #21857, .T. ) ;
#14446=CARTESIAN_POINT ( 'NONE',  ( -14.71174975910705029, 50.19799549595485644, 13.75000000000000000 ) ) ;
#14482=DIRECTION ( 'NONE',  ( -1.000000000000000000, 0.000000000000000000, 0.000000000000000000 ) ) ;
#14542=DIRECTION ( 'NONE',  ( -0.000000000000000000, -0.000000000000000000, 1.000000000000000000 ) ) ;
#14658=CIRCLE ( 'NONE', #10407, 0.2500000000000002220 ) ;
#14675=EDGE_CURVE ( 'NONE', #18906, #1545, #7570, .T. ) ;
#14678=EDGE_LOOP ( 'NONE', ( #7, #15301, #4014, #10146 ) ) ;
#14683=AXIS2_PLACEMENT_3D ( 'NONE', #5210, #17171, #58 ) ;
#14930=AXIS2_PLACEMENT_3D ( 'NONE', #9956, #11728, #8617 ) ;
#14953=ORIENTED_EDGE ( 'NONE', *, *, #18857, .F. ) ;
#14957=VECTOR ( 'NONE', #3343, 1000.000000000000000 ) ;
#14959=ADVANCED_FACE ( 'NONE', ( #1890 ), #8388, .T. ) ;
#15097=VECTOR ( 'NONE', #13766, 1000.000000000000000 ) ;
#15119=CARTESIAN_POINT ( 'NONE',  ( -14.71174975910705029, 51.61873716947361856, 13.50000000000000000 ) ) ;
#15172=ORIENTED_EDGE ( 'NONE', *, *, #20828, .F. ) ;
#15219=DIRECTION ( 'NONE',  ( -1.000000000000000000, -0.000000000000000000, 2.388292521039847891E-16 ) ) ;
#15236=ORIENTED_EDGE ( 'NONE', *, *, #5123, .T. ) ;
#15256=ORIENTED_EDGE ( 'NONE', *, *, #4274, .T. ) ;
#15258=AXIS2_PLACEMENT_3D ( 'NONE', #20116, #11580, #12025 ) ;
#15301=ORIENTED_EDGE ( 'NONE', *, *, #2564, .T. ) ;
#15323=ADVANCED_FACE ( 'NONE', ( #11594 ), #9942, .T. ) ;
#15338=DIRECTION ( 'NONE',  ( 0.000000000000000000, 0.000000000000000000, -1.000000000000000000 ) ) ;
#15342=CARTESIAN_POINT ( 'NONE',  ( 14.71174975910705740, 51.61873716947361856, 14.00000000000000000 ) ) ;
#15352=PLANE ( 'NONE',  #6488 ) ;
#15409=DIRECTION ( 'NONE',  ( -0.000000000000000000, -0.000000000000000000, -1.000000000000000000 ) ) ;
#15475=ORIENTED_EDGE ( 'NONE', *, *, #3199, .T. ) ;
#15603=EDGE_CURVE ( 'NONE', #8454, #18731, #20893, .T. ) ;
#15719=STYLED_ITEM ( 'NONE', ( #16693 ), #20415 ) ;
#15728=ORIENTED_EDGE ( 'NONE', *, *, #19930, .T. ) ;
#15882=VECTOR ( 'NONE', #13398, 1000.000000000000000 ) ;
#15954=CARTESIAN_POINT ( 'NONE',  ( 14.71174975910706983, 52.11873716947361856, 68.00000000000000000 ) ) ;
#15982=CIRCLE ( 'NONE', #13835, 0.2500000000000002220 ) ;
#16012=TOROIDAL_SURFACE ( 'NONE', #18905, 0.2500000000000000000, 0.2500000000000000000 ) ;
#16179=ADVANCED_FACE ( 'NONE', ( #19840 ), #16361, .T. ) ;
#16226=DIRECTION ( 'NONE',  ( 1.000000000000000000, 0.000000000000000000, 0.000000000000000000 ) ) ;
#16255=CARTESIAN_POINT ( 'NONE',  ( -14.96174975910705207, 42.31054587065082728, 13.75000000000000000 ) ) ;
#16315=ADVANCED_BREP_SHAPE_REPRESENTATION ( '', ( #20415, #17493 ), #19794 ) ;
#16335=CARTESIAN_POINT ( 'NONE',  ( -14.71174975910705029, 52.11873716947361856, 68.00000000000000000 ) ) ;
#16361=PLANE ( 'NONE',  #22054 ) ;
#16425=EDGE_CURVE ( 'NONE', #2099, #5378, #21330, .T. ) ;
#16590=PRODUCT ( 'Glass Cover', 'Glass Cover', '', ( #2464 ) ) ;
#16618=TOROIDAL_SURFACE ( 'NONE', #10906, 0.2500000000000000000, 0.2500000000000000000 ) ;
#16630=DIRECTION ( 'NONE',  ( 1.000000000000000000, 0.000000000000000000, -2.388292521039847891E-16 ) ) ;
#16677=CARTESIAN_POINT ( 'NONE',  ( 14.71174975910707161, 0.000000000000000000, 68.25000000000000000 ) ) ;
#16693=PRESENTATION_STYLE_ASSIGNMENT (( #17930 ) ) ;
#16712=EDGE_CURVE ( 'NONE', #18906, #17812, #5267, .T. ) ;
#16715=LINE ( 'NONE', #2624, #19536 ) ;
#16729=FACE_OUTER_BOUND ( 'NONE', #1131, .T. ) ;
#16770=EDGE_CURVE ( 'NONE', #2469, #2743, #3117, .T. ) ;
#16803=LINE ( 'NONE', #15119, #12693 ) ;
#16889=DIRECTION ( 'NONE',  ( 0.000000000000000000, -1.000000000000000000, 0.000000000000000000 ) ) ;
#16902=DIRECTION ( 'NONE',  ( 0.000000000000000000, -1.000000000000000000, 0.000000000000000000 ) ) ;
#16904=ORIENTED_EDGE ( 'NONE', *, *, #16770, .T. ) ;
#16977=CARTESIAN_POINT ( 'NONE',  ( 14.71174975910706451, 50.19799549595485644, 68.50000000000000000 ) ) ;
#17043=ORIENTED_EDGE ( 'NONE', *, *, #11090, .T. ) ;
#17065=DIRECTION ( 'NONE',  ( 0.000000000000000000, -0.000000000000000000, 1.000000000000000000 ) ) ;
#17092=EDGE_CURVE ( 'NONE', #1545, #1750, #15982, .T. ) ;
#17120=AXIS2_PLACEMENT_3D ( 'NONE', #14380, #12587, #9036 ) ;
#17171=DIRECTION ( 'NONE',  ( 0.000000000000000000, 0.000000000000000000, 1.000000000000000000 ) ) ;
#17175=VERTEX_POINT ( 'NONE', #13458 ) ;
#17186=EDGE_CURVE ( 'NONE', #21823, #12212, #20298, .T. ) ;
#17277=CARTESIAN_POINT ( 'NONE',  ( -14.71174975910705029, 51.61873716947361856, 14.00000000000000000 ) ) ;
#17443=UNCERTAINTY_MEASURE_WITH_UNIT (LENGTH_MEASURE( 1.000000000000000082E-05 ), #5320, 'distance_accuracy_value', 'NONE');
#17493=AXIS2_PLACEMENT_3D ( 'NONE', #9767, #1237, #16226 ) ;
#17544=EDGE_CURVE ( 'NONE', #1750, #17812, #19236, .T. ) ;
#17555=ADVANCED_FACE ( 'NONE', ( #5169 ), #9229, .T. ) ;
#17557=AXIS2_PLACEMENT_3D ( 'NONE', #17277, #19080, #1942 ) ;
#17591=ADVANCED_FACE ( 'NONE', ( #8528 ), #10097, .T. ) ;
#17593=ORIENTED_EDGE ( 'NONE', *, *, #1216, .T. ) ;
#17639=( GEOMETRIC_REPRESENTATION_CONTEXT ( 3 ) GLOBAL_UNCERTAINTY_ASSIGNED_CONTEXT ( ( #13856 ) ) GLOBAL_UNIT_ASSIGNED_CONTEXT ( ( #7209, #12309, #18022 ) ) REPRESENTATION_CONTEXT ( 'NONE', 'WORKASPACE' ) );
#17801=DIRECTION ( 'NONE',  ( -1.000000000000000000, -0.000000000000000000, -0.000000000000000000 ) ) ;
#17812=VERTEX_POINT ( 'NONE', #4137 ) ;
#17847=CARTESIAN_POINT ( 'NONE',  ( 0.000000000000000000, 50.19799549595485644, 13.50000000000000000 ) ) ;
#17865=DIRECTION ( 'NONE',  ( 0.000000000000000000, -1.000000000000000000, 0.000000000000000000 ) ) ;
#17930=SURFACE_STYLE_USAGE ( .BOTH. , #11444 ) ;
#18020=ORIENTED_EDGE ( 'NONE', *, *, #20381, .F. ) ;
#18022=( NAMED_UNIT ( * ) SI_UNIT ( $, .STERADIAN. ) SOLID_ANGLE_UNIT ( ) );
#18060=VECTOR ( 'NONE', #2417, 1000.000000000000000 ) ;
#18154=LINE ( 'NONE', #9672, #9294 ) ;
#18161=ORIENTED_EDGE ( 'NONE', *, *, #16425, .F. ) ;
#18194=DIRECTION ( 'NONE',  ( 1.000000000000000000, 0.000000000000000000, 0.000000000000000000 ) ) ;
#18361=DIRECTION ( 'NONE',  ( 0.000000000000000000, 0.000000000000000000, 1.000000000000000000 ) ) ;
#18473=DIRECTION ( 'NONE',  ( 0.000000000000000000, 0.000000000000000000, -1.000000000000000000 ) ) ;
#18516=AXIS2_PLACEMENT_3D ( 'NONE', #12807, #6127, #13016 ) ;
#18635=EDGE_LOOP ( 'NONE', ( #19852, #21124, #18161, #8109 ) ) ;
#18681=DIRECTION ( 'NONE',  ( 0.000000000000000000, 0.000000000000000000, -1.000000000000000000 ) ) ;
#18711=DIRECTION ( 'NONE',  ( 0.000000000000000000, 0.000000000000000000, 1.000000000000000000 ) ) ;
#18731=VERTEX_POINT ( 'NONE', #4203 ) ;
#18813=CARTESIAN_POINT ( 'NONE',  ( -14.71174975910705029, 51.61873716947361856, 68.00000000000000000 ) ) ;
#18828=DIRECTION ( 'NONE',  ( -0.000000000000000000, 1.000000000000000000, 0.000000000000000000 ) ) ;
#18857=EDGE_CURVE ( 'NONE', #2743, #19660, #6122, .T. ) ;
#18905=AXIS2_PLACEMENT_3D ( 'NONE', #2154, #5646, #14007 ) ;
#18906=VERTEX_POINT ( 'NONE', #19864 ) ;
#18917=CARTESIAN_POINT ( 'NONE',  ( 14.71174975910705740, 32.10873716947361345, 13.75000000000000000 ) ) ;
#18937=ORIENTED_EDGE ( 'NONE', *, *, #17544, .F. ) ;
#18976=CARTESIAN_POINT ( 'NONE',  ( -14.96174975910705207, 51.86873716947361856, 68.00000000000000000 ) ) ;
#19061=SURFACE_SIDE_STYLE ('',( #20749 ) ) ;
#19080=DIRECTION ( 'NONE',  ( 1.000000000000000000, -0.000000000000000000, -0.000000000000000000 ) ) ;
#19112=ORIENTED_EDGE ( 'NONE', *, *, #20614, .T. ) ;
#19116=EDGE_CURVE ( 'NONE', #21318, #1488, #20426, .T. ) ;
#19164=ORIENTED_EDGE ( 'NONE', *, *, #3097, .F. ) ;
#19171=CIRCLE ( 'NONE', #10939, 0.2500000000000002220 ) ;
#19213=DIRECTION ( 'NONE',  ( 1.000000000000000000, 0.000000000000000000, -0.000000000000000000 ) ) ;
#19236=CIRCLE ( 'NONE', #3520, 0.5000000000000004441 ) ;
#19270=DIRECTION ( 'NONE',  ( -1.000000000000000000, -0.000000000000000000, 2.388292521039847891E-16 ) ) ;
#19310=ORIENTED_EDGE ( 'NONE', *, *, #520, .T. ) ;
#19358=CARTESIAN_POINT ( 'NONE',  ( 14.71174975910705740, 51.61873716947361856, 14.00000000000000000 ) ) ;
#19421=PRODUCT_DEFINITION ( 'UNKNOWN', '', #490, #8412 ) ;
#19439=CYLINDRICAL_SURFACE ( 'NONE', #11699, 0.2500000000000002220 ) ;
#19536=VECTOR ( 'NONE', #21780, 1000.000000000000000 ) ;
#19544=CARTESIAN_POINT ( 'NONE',  ( 14.71174975910705740, 50.19799549595485644, 13.75000000000000000 ) ) ;
#19549=DIRECTION ( 'NONE',  ( 0.000000000000000000, 0.000000000000000000, -1.000000000000000000 ) ) ;
#19660=VERTEX_POINT ( 'NONE', #11415 ) ;
#19794=( GEOMETRIC_REPRESENTATION_CONTEXT ( 3 ) GLOBAL_UNCERTAINTY_ASSIGNED_CONTEXT ( ( #17443 ) ) GLOBAL_UNIT_ASSIGNED_CONTEXT ( ( #5320, #11888, #1714 ) ) REPRESENTATION_CONTEXT ( 'NONE', 'WORKASPACE' ) );
#19840=FACE_OUTER_BOUND ( 'NONE', #21657, .T. ) ;
#19852=ORIENTED_EDGE ( 'NONE', *, *, #356, .T. ) ;
#19853=DIRECTION ( 'NONE',  ( 1.000000000000000000, 0.000000000000000000, 0.000000000000000000 ) ) ;
#19864=CARTESIAN_POINT ( 'NONE',  ( 14.96174975910705918, 51.61873716947361856, 13.75000000000000000 ) ) ;
#19930=EDGE_CURVE ( 'NONE', #21823, #21318, #576, .T. ) ;
#19967=SURFACE_STYLE_FILL_AREA ( #7988 ) ;
#19972=ORIENTED_EDGE ( 'NONE', *, *, #2999, .T. ) ;
#19974=CIRCLE ( 'NONE', #18516, 0.2500000000000002220 ) ;
#19980=CARTESIAN_POINT ( 'NONE',  ( 14.71174975910705740, 51.86873716947361856, 14.00000000000000000 ) ) ;
#20013=VECTOR ( 'NONE', #9750, 1000.000000000000000 ) ;
#20043=DIRECTION ( 'NONE',  ( 0.000000000000000000, 0.000000000000000000, 1.000000000000000000 ) ) ;
#20057=ORIENTED_EDGE ( 'NONE', *, *, #20465, .F. ) ;
#20116=CARTESIAN_POINT ( 'NONE',  ( 14.71174975910705740, 51.61873716947361856, 13.75000000000000000 ) ) ;
#20199=CARTESIAN_POINT ( 'NONE',  ( 14.71174975910707161, 0.000000000000000000, 68.50000000000000000 ) ) ;
#20203=PLANE ( 'NONE',  #10566 ) ;
#20292=AXIS2_PLACEMENT_3D ( 'NONE', #8287, #21937, #6613 ) ;
#20298=LINE ( 'NONE', #21879, #8141 ) ;
#20365=ORIENTED_EDGE ( 'NONE', *, *, #11090, .F. ) ;
#20381=EDGE_CURVE ( 'NONE', #11094, #1177, #18154, .T. ) ;
#20407=FACE_OUTER_BOUND ( 'NONE', #4080, .T. ) ;
#20415=MANIFOLD_SOLID_BREP ( 'Stock-MAS-696-1', #264 ) ;
#20426=LINE ( 'NONE', #5095, #4538 ) ;
#20429=EDGE_LOOP ( 'NONE', ( #138, #6637, #1723, #3850 ) ) ;
#20465=EDGE_CURVE ( 'NONE', #19660, #18731, #12, .T. ) ;
#20523=SURFACE_STYLE_USAGE ( .BOTH. , #19061 ) ;
#20555=ADVANCED_FACE ( 'NONE', ( #20407 ), #15352, .T. ) ;
#20569=PLANE ( 'NONE',  #5158 ) ;
#20607=EDGE_LOOP ( 'NONE', ( #20365, #15172, #8725, #4552 ) ) ;
#20614=EDGE_CURVE ( 'NONE', #12641, #6442, #14658, .T. ) ;
#20621=CIRCLE ( 'NONE', #12722, 0.2500000000000002220 ) ;
#20630=AXIS2_PLACEMENT_3D ( 'NONE', #3425, #8697, #13702 ) ;
#20654=CYLINDRICAL_SURFACE ( 'NONE', #14683, 0.2500000000000002220 ) ;
#20700=AXIS2_PLACEMENT_3D ( 'NONE', #4582, #21495, #768 ) ;
#20737=( GEOMETRIC_REPRESENTATION_CONTEXT ( 3 ) GLOBAL_UNCERTAINTY_ASSIGNED_CONTEXT ( ( #13097 ) ) GLOBAL_UNIT_ASSIGNED_CONTEXT ( ( #21644, #1368, #9775 ) ) REPRESENTATION_CONTEXT ( 'NONE', 'WORKASPACE' ) );
#20749=SURFACE_STYLE_FILL_AREA ( #13899 ) ;
#20761=CARTESIAN_POINT ( 'NONE',  ( -14.96174975910705207, 51.61873716947361856, 13.75000000000000000 ) ) ;
#20794=CARTESIAN_POINT ( 'NONE',  ( 14.71174975910705740, 52.11873716947361856, 14.00000000000000000 ) ) ;
#20797=PLANE ( 'NONE',  #20923 ) ;
#20828=EDGE_CURVE ( 'NONE', #17812, #8454, #2687, .T. ) ;
#20893=LINE ( 'NONE', #17847, #18060 ) ;
#20896=PLANE ( 'NONE',  #7825 ) ;
#20923=AXIS2_PLACEMENT_3D ( 'NONE', #5476, #14055, #18194 ) ;
#20960=ORIENTED_EDGE ( 'NONE', *, *, #3916, .F. ) ;
#20987=EDGE_LOOP ( 'NONE', ( #6327, #3075, #12336, #20960 ) ) ;
#21019=CARTESIAN_POINT ( 'NONE',  ( -14.71174975910705029, 52.11873716947361856, 109.6002446535588319 ) ) ;
#21023=ORIENTED_EDGE ( 'NONE', *, *, #15603, .F. ) ;
#21032=AXIS2_PLACEMENT_3D ( 'NONE', #18813, #8406, #13659 ) ;
#21083=SHAPE_REPRESENTATION_RELATIONSHIP ( 'NONE' , 'NONE' ,  #6277, #16315 ) ;
#21124=ORIENTED_EDGE ( 'NONE', *, *, #5123, .F. ) ;
#21225=LINE ( 'NONE', #9455, #5447 ) ;
#21304=DIRECTION ( 'NONE',  ( -1.000000000000000000, 0.000000000000000000, 0.000000000000000000 ) ) ;
#21318=VERTEX_POINT ( 'NONE', #495 ) ;
#21330=CIRCLE ( 'NONE', #10264, 0.2500000000000002220 ) ;
#21332=DIRECTION ( 'NONE',  ( 0.000000000000000000, -1.000000000000000000, 0.000000000000000000 ) ) ;
#21372=ORIENTED_EDGE ( 'NONE', *, *, #12018, .F. ) ;
#21411=ORIENTED_EDGE ( 'NONE', *, *, #17092, .F. ) ;
#21495=DIRECTION ( 'NONE',  ( 0.000000000000000000, 1.000000000000000000, -0.000000000000000000 ) ) ;
#21524=AXIS2_PLACEMENT_3D ( 'NONE', #9440, #12892, #21650 ) ;
#21537=DIRECTION ( 'NONE',  ( 0.000000000000000000, 0.000000000000000000, 1.000000000000000000 ) ) ;
#21629=PRODUCT_DEFINITION_SHAPE ( 'NONE', 'NONE',  #19421 ) ;
#21644=( LENGTH_UNIT ( ) NAMED_UNIT ( * ) SI_UNIT ( .MILLI., .METRE. ) );
#21650=DIRECTION ( 'NONE',  ( 0.000000000000000000, 0.000000000000000000, -1.000000000000000000 ) ) ;
#21657=EDGE_LOOP ( 'NONE', ( #15475, #6603, #19112, #8362, #16904, #12562 ) ) ;
#21698=CARTESIAN_POINT ( 'NONE',  ( -14.71174975910705029, 51.86873716947361856, 68.00000000000000000 ) ) ;
#21734=LINE ( 'NONE', #4609, #12577 ) ;
#21770=CIRCLE ( 'NONE', #20700, 0.2500000000000002220 ) ;
#21780=DIRECTION ( 'NONE',  ( 1.000000000000000000, 0.000000000000000000, -0.000000000000000000 ) ) ;
#21791=CARTESIAN_POINT ( 'NONE',  ( -14.96174975910705207, 50.19799549595485644, -3.500000000000003109 ) ) ;
#21823=VERTEX_POINT ( 'NONE', #16335 ) ;
#21857=CIRCLE ( 'NONE', #17557, 0.5000000000000004441 ) ;
#21879=CARTESIAN_POINT ( 'NONE',  ( 0.000000000000000000, 52.11873716947361856, 68.00000000000000000 ) ) ;
#21937=DIRECTION ( 'NONE',  ( -0.000000000000000000, -1.000000000000000000, -0.000000000000000000 ) ) ;
#21961=DIRECTION ( 'NONE',  ( 0.000000000000000000, 1.000000000000000000, 0.000000000000000000 ) ) ;
#22054=AXIS2_PLACEMENT_3D ( 'NONE', #7887, #21304, #21537 ) ;
#22057=CARTESIAN_POINT ( 'NONE',  ( 14.71174975910707161, 51.61873716947361856, 68.50000000000000000 ) ) ;
#22126=DIRECTION ( 'NONE',  ( -0.000000000000000000, 1.000000000000000000, 0.000000000000000000 ) ) ;
ENDSEC;
END-ISO-10303-21;
